ISO-10303-21;
HEADER;
FILE_DESCRIPTION (('STEP AP214'),
    '1' );
FILE_NAME ('socket head cap screw_iso_ISO 4762 M5 x 25 - 25N.step',
    '2026-10-31T03:46:07',
    ( '' ),
    ( '' ),
    'SwSTEP 2.0',
    'SolidWorks 2026',
    '' );
FILE_SCHEMA (( 'AUTOMOTIVE_DESIGN' ));
ENDSEC;

DATA;
#43=CARTESIAN_POINT ( 'NONE',  ( 0.000000000000000000, 1.178949249685218970, 2.041999999999998483 ) ) ;
#53=LINE ( 'NONE', #5589, #20648 ) ;
#81=DIRECTION ( 'NONE',  ( 1.000000000000000000, 0.000000000000000000, 0.000000000000000000 ) ) ;
#123=ORIENTED_EDGE ( 'NONE', *, *, #13032, .T. ) ;
#156=CARTESIAN_POINT ( 'NONE',  ( 5.000000000000015099, 0.000000000000000000, 0.000000000000000000 ) ) ;
#163=DIRECTION ( 'NONE',  ( 1.000000000000000000, 0.000000000000000000, 0.000000000000000000 ) ) ;
#187=ORIENTED_EDGE ( 'NONE', *, *, #21854, .T. ) ;
#322=ADVANCED_FACE ( 'NONE', ( #4811 ), #10520, .T. ) ;
#422=VERTEX_POINT ( 'NONE', #11864 ) ;
#451=FILL_AREA_STYLE ('',( #1678 ) ) ;
#510=ADVANCED_FACE ( 'NONE', ( #8805 ), #10215, .F. ) ;
#525=CARTESIAN_POINT ( 'NONE',  ( 5.200000000000020606, 0.000000000000000000, 2.499999999999993339 ) ) ;
#553=CARTESIAN_POINT ( 'NONE',  ( 0.000000000000000000, 2.357898499370434386, -3.469446951953614189E-15 ) ) ;
#588=( GEOMETRIC_REPRESENTATION_CONTEXT ( 3 ) GLOBAL_UNCERTAINTY_ASSIGNED_CONTEXT ( ( #4447 ) ) GLOBAL_UNIT_ASSIGNED_CONTEXT ( ( #9575, #6058, #2789 ) ) REPRESENTATION_CONTEXT ( 'NONE', 'WORKASPACE' ) );
#623=EDGE_CURVE ( 'NONE', #21238, #949, #17113, .T. ) ;
#683=DIRECTION ( 'NONE',  ( 0.000000000000000000, 1.103561164596346103E-15, 1.000000000000000000 ) ) ;
#705=ADVANCED_FACE ( 'NONE', ( #14000 ), #23134, .F. ) ;
#914=AXIS2_PLACEMENT_3D ( 'NONE', #2286, #9683, #4344 ) ;
#922=DIRECTION ( 'NONE',  ( 0.000000000000000000, 0.5000000000000009992, 0.8660254037844380415 ) ) ;
#949=VERTEX_POINT ( 'NONE', #11659 ) ;
#960=AXIS2_PLACEMENT_3D ( 'NONE', #15591, #5069, #17857 ) ;
#969=ORIENTED_EDGE ( 'NONE', *, *, #12126, .F. ) ;
#1010=VECTOR ( 'NONE', #22140, 1000.000000000000114 ) ;
#1056=CARTESIAN_POINT ( 'NONE',  ( 2.500000000000002220, -1.178949249685218970, -2.041999999999998483 ) ) ;
#1062=AXIS2_PLACEMENT_3D ( 'NONE', #23583, #7039, #5346 ) ;
#1079=EDGE_LOOP ( 'NONE', ( #23639, #11251, #9429 ) ) ;
#1120=CIRCLE ( 'NONE', #22717, 4.000000000000000000 ) ;
#1122=DIRECTION ( 'NONE',  ( 0.000000000000000000, 0.000000000000000000, -1.000000000000000000 ) ) ;
#1129=PLANE ( 'NONE',  #19628 ) ;
#1153=DIRECTION ( 'NONE',  ( 0.000000000000000000, 0.000000000000000000, 1.000000000000000000 ) ) ;
#1169=ORIENTED_EDGE ( 'NONE', *, *, #6665, .F. ) ;
#1208=CARTESIAN_POINT ( 'NONE',  ( 2.500000000000002220, 0.000000000000000000, 0.000000000000000000 ) ) ;
#1242=ADVANCED_FACE ( 'NONE', ( #18343 ), #9189, .F. ) ;
#1260=LINE ( 'NONE', #1491, #9578 ) ;
#1357=DIRECTION ( 'NONE',  ( -1.000000000000000000, 0.000000000000000000, 0.000000000000000000 ) ) ;
#1380=CARTESIAN_POINT ( 'NONE',  ( -31.74999999999994316, 5.204748896376250699E-16, -4.250000000000000000 ) ) ;
#1382=EDGE_LOOP ( 'NONE', ( #20054, #9582 ) ) ;
#1416=ORIENTED_EDGE ( 'NONE', *, *, #21211, .F. ) ;
#1439=EDGE_CURVE ( 'NONE', #22213, #6889, #13436, .T. ) ;
#1491=CARTESIAN_POINT ( 'NONE',  ( -31.74999999999994316, 0.000000000000000000, 4.250000000000000000 ) ) ;
#1511=VECTOR ( 'NONE', #22387, 1000.000000000000114 ) ;
#1544=EDGE_LOOP ( 'NONE', ( #23507, #23295, #21687 ) ) ;
#1549=ORIENTED_EDGE ( 'NONE', *, *, #14515, .T. ) ;
#1554=EDGE_CURVE ( 'NONE', #23349, #12522, #2502, .T. ) ;
#1678=FILL_AREA_STYLE_COLOUR ( '', #3815 ) ;
#1743=LINE ( 'NONE', #15064, #4801 ) ;
#1758=EDGE_CURVE ( 'NONE', #10543, #11584, #3381, .T. ) ;
#1769=DIRECTION ( 'NONE',  ( 0.000000000000000000, 0.000000000000000000, 1.000000000000000000 ) ) ;
#1850=EDGE_CURVE ( 'NONE', #11584, #22213, #9574, .T. ) ;
#1877=DIRECTION ( 'NONE',  ( -1.000000000000000000, 0.000000000000000000, 0.000000000000000000 ) ) ;
#1942=PLANE ( 'NONE',  #4124 ) ;
#1954=EDGE_LOOP ( 'NONE', ( #7032, #3935, #21847, #5928, #4847 ) ) ;
#1963=VERTEX_POINT ( 'NONE', #12446 ) ;
#2065=EDGE_LOOP ( 'NONE', ( #6823, #9129 ) ) ;
#2066=EDGE_CURVE ( 'NONE', #3824, #11584, #7536, .T. ) ;
#2072=DIRECTION ( 'NONE',  ( 0.000000000000000000, -0.5000000000000009992, -0.8660254037844380415 ) ) ;
#2150=VERTEX_POINT ( 'NONE', #22389 ) ;
#2209=CIRCLE ( 'NONE', #15734, 2.500000000000000888 ) ;
#2241=EDGE_CURVE ( 'NONE', #13509, #22474, #19838, .T. ) ;
#2286=CARTESIAN_POINT ( 'NONE',  ( 2.500000000000002220, 0.000000000000000000, 0.000000000000000000 ) ) ;
#2305=PRODUCT_DEFINITION_FORMATION_WITH_SPECIFIED_SOURCE ( 'ANY', '', #12733, .NOT_KNOWN. ) ;
#2409=EDGE_CURVE ( 'NONE', #2150, #23349, #8623, .T. ) ;
#2411=EDGE_CURVE ( 'NONE', #17092, #2150, #3631, .T. ) ;
#2502=CIRCLE ( 'NONE', #960, 2.500000000000000444 ) ;
#2514=ADVANCED_FACE ( 'NONE', ( #14665, #5002 ), #19716, .T. ) ;
#2533=PLANE ( 'NONE',  #8822 ) ;
#2556=EDGE_LOOP ( 'NONE', ( #1169, #20317, #11260, #17051 ) ) ;
#2560=CARTESIAN_POINT ( 'NONE',  ( 0.2500000000000002220, 5.204748896376238866E-16, -4.249999999999979572 ) ) ;
#2593=AXIS2_PLACEMENT_3D ( 'NONE', #14134, #8673, #5060 ) ;
#2600=ORIENTED_EDGE ( 'NONE', *, *, #4041, .F. ) ;
#2761=CARTESIAN_POINT ( 'NONE',  ( -31.74999999999994316, 0.000000000000000000, 0.000000000000000000 ) ) ;
#2768=EDGE_LOOP ( 'NONE', ( #20010, #7873, #12545, #10162, #19871 ) ) ;
#2789=( NAMED_UNIT ( * ) SI_UNIT ( $, .STERADIAN. ) SOLID_ANGLE_UNIT ( ) );
#2790=ORIENTED_EDGE ( 'NONE', *, *, #2409, .T. ) ;
#2882=VERTEX_POINT ( 'NONE', #9889 ) ;
#2942=CYLINDRICAL_SURFACE ( 'NONE', #22654, 2.500000000000000444 ) ;
#2945=VECTOR ( 'NONE', #21265, 1000.000000000000000 ) ;
#3008=ORIENTED_EDGE ( 'NONE', *, *, #4358, .T. ) ;
#3060=DIRECTION ( 'NONE',  ( -1.000000000000000000, 0.000000000000000000, 0.000000000000000000 ) ) ;
#3071=FACE_OUTER_BOUND ( 'NONE', #15603, .T. ) ;
#3087=VECTOR ( 'NONE', #7219, 1000.000000000000000 ) ;
#3121=ORIENTED_EDGE ( 'NONE', *, *, #14762, .F. ) ;
#3184=DIRECTION ( 'NONE',  ( -1.000000000000000000, 0.000000000000000000, 0.000000000000000000 ) ) ;
#3208=CARTESIAN_POINT ( 'NONE',  ( 2.500000000000002220, 2.357898499370434386, -3.469446951953614189E-15 ) ) ;
#3209=EDGE_CURVE ( 'NONE', #4361, #20959, #18133, .T. ) ;
#3256=ORIENTED_EDGE ( 'NONE', *, *, #18134, .T. ) ;
#3261=CARTESIAN_POINT ( 'NONE',  ( 2.500000000000002220, 1.178949249685212086, -2.042000000000002036 ) ) ;
#3276=EDGE_CURVE ( 'NONE', #12504, #22000, #21221, .T. ) ;
#3349=ADVANCED_FACE ( 'NONE', ( #19830 ), #17327, .T. ) ;
#3359=LINE ( 'NONE', #23763, #3087 ) ;
#3381=CIRCLE ( 'NONE', #14239, 2.041999999999999815 ) ;
#3457=LINE ( 'NONE', #19877, #13912 ) ;
#3516=ORIENTED_EDGE ( 'NONE', *, *, #21211, .T. ) ;
#3532=DIRECTION ( 'NONE',  ( 0.000000000000000000, 0.000000000000000000, 1.000000000000000000 ) ) ;
#3552=ORIENTED_EDGE ( 'NONE', *, *, #17868, .F. ) ;
#3562=FACE_BOUND ( 'NONE', #2065, .T. ) ;
#3584=CARTESIAN_POINT ( 'NONE',  ( 0.000000000000000000, 0.000000000000000000, 4.000000000000000000 ) ) ;
#3631=LINE ( 'NONE', #16455, #1511 ) ;
#3676=CARTESIAN_POINT ( 'NONE',  ( 5.000000000000015099, 4.250000000000000000, 0.000000000000000000 ) ) ;
#3680=VECTOR ( 'NONE', #11302, 1000.000000000000000 ) ;
#3690=ORIENTED_EDGE ( 'NONE', *, *, #5895, .T. ) ;
#3702=FACE_OUTER_BOUND ( 'NONE', #21428, .T. ) ;
#3714=ORIENTED_EDGE ( 'NONE', *, *, #5895, .F. ) ;
#3758=AXIS2_PLACEMENT_3D ( 'NONE', #20221, #81, #16737 ) ;
#3769=DIRECTION ( 'NONE',  ( 1.000000000000000000, 0.000000000000000000, 0.000000000000000000 ) ) ;
#3791=AXIS2_PLACEMENT_3D ( 'NONE', #10591, #8636, #16123 ) ;
#3815=COLOUR_RGB ( '',1.000000000000000000, 0.9490196078431372140, 0.9098039215686274384 ) ;
#3821=AXIS2_PLACEMENT_3D ( 'NONE', #156, #16456, #22223 ) ;
#3823=ADVANCED_FACE ( 'NONE', ( #19590 ), #1129, .F. ) ;
#3824=VERTEX_POINT ( 'NONE', #16112 ) ;
#3893=LINE ( 'NONE', #21247, #3680 ) ;
#3914=DIRECTION ( 'NONE',  ( 0.000000000000000000, 1.000000000000000000, -1.103561164596346103E-15 ) ) ;
#3927=ORIENTED_EDGE ( 'NONE', *, *, #1439, .T. ) ;
#3935=ORIENTED_EDGE ( 'NONE', *, *, #8444, .F. ) ;
#3954=CONICAL_SURFACE ( 'NONE', #8620, 2.041999999999999815, 1.047197551196591858 ) ;
#3960=EDGE_CURVE ( 'NONE', #19049, #18989, #9619, .T. ) ;
#3961=ORIENTED_EDGE ( 'NONE', *, *, #5807, .T. ) ;
#3991=EDGE_LOOP ( 'NONE', ( #8643, #19958, #17018, #19670, #20568 ) ) ;
#4026=VECTOR ( 'NONE', #15085, 1000.000000000000114 ) ;
#4037=AXIS2_PLACEMENT_3D ( 'NONE', #15336, #22551, #16889 ) ;
#4041=EDGE_CURVE ( 'NONE', #22474, #22000, #1120, .T. ) ;
#4061=ORIENTED_EDGE ( 'NONE', *, *, #22012, .T. ) ;
#4076=MANIFOLD_SOLID_BREP ( 'Hex', #15270 ) ;
#4111=ORIENTED_EDGE ( 'NONE', *, *, #13335, .T. ) ;
#4117=CARTESIAN_POINT ( 'NONE',  ( 0.000000000000000000, 0.000000000000000000, 0.000000000000000000 ) ) ;
#4122=AXIS2_PLACEMENT_3D ( 'NONE', #23776, #7233, #21971 ) ;
#4124=AXIS2_PLACEMENT_3D ( 'NONE', #9441, #16795, #16684 ) ;
#4199=AXIS2_PLACEMENT_3D ( 'NONE', #9108, #10835, #3532 ) ;
#4344=DIRECTION ( 'NONE',  ( 0.000000000000000000, 0.000000000000000000, 1.000000000000000000 ) ) ;
#4349=DIRECTION ( 'NONE',  ( 1.000000000000000000, 0.000000000000000000, 0.000000000000000000 ) ) ;
#4358=EDGE_CURVE ( 'NONE', #949, #10801, #9071, .T. ) ;
#4361=VERTEX_POINT ( 'NONE', #12852 ) ;
#4363=ORIENTED_EDGE ( 'NONE', *, *, #12194, .F. ) ;
#4406=CARTESIAN_POINT ( 'NONE',  ( 5.000000000000015099, 0.000000000000000000, 0.000000000000000000 ) ) ;
#4447=UNCERTAINTY_MEASURE_WITH_UNIT (LENGTH_MEASURE( 1.000000000000000082E-05 ), #9575, 'distance_accuracy_value', 'NONE');
#4538=VERTEX_POINT ( 'NONE', #23040 ) ;
#4612=DIRECTION ( 'NONE',  ( 0.000000000000000000, -1.000000000000000000, 1.287488025362403787E-15 ) ) ;
#4700=ORIENTED_EDGE ( 'NONE', *, *, #17868, .T. ) ;
#4716=VECTOR ( 'NONE', #18702, 1000.000000000000000 ) ;
#4722=CARTESIAN_POINT ( 'NONE',  ( 0.000000000000000000, 1.178949249685212086, -2.042000000000002036 ) ) ;
#4768=DIRECTION ( 'NONE',  ( 0.000000000000000000, 0.000000000000000000, 1.000000000000000000 ) ) ;
#4801=VECTOR ( 'NONE', #3914, 1000.000000000000000 ) ;
#4811=FACE_OUTER_BOUND ( 'NONE', #22863, .T. ) ;
#4847=ORIENTED_EDGE ( 'NONE', *, *, #5152, .T. ) ;
#4886=CARTESIAN_POINT ( 'NONE',  ( 30.00000000000000000, 0.000000000000000000, 2.054999999999993054 ) ) ;
#4911=CARTESIAN_POINT ( 'NONE',  ( 0.000000000000000000, 2.357898499370434386, -3.469446951953614189E-15 ) ) ;
#4969=CIRCLE ( 'NONE', #3791, 2.500000000000000888 ) ;
#4984=VECTOR ( 'NONE', #17345, 1000.000000000000114 ) ;
#4995=ADVANCED_FACE ( 'NONE', ( #10470 ), #16057, .T. ) ;
#5002=FACE_OUTER_BOUND ( 'NONE', #7347, .T. ) ;
#5024=ORIENTED_EDGE ( 'NONE', *, *, #18551, .T. ) ;
#5033=CIRCLE ( 'NONE', #10063, 2.700000000000000622 ) ;
#5055=FACE_OUTER_BOUND ( 'NONE', #1079, .T. ) ;
#5060=DIRECTION ( 'NONE',  ( 0.000000000000000000, 0.000000000000000000, -1.000000000000000000 ) ) ;
#5069=DIRECTION ( 'NONE',  ( 1.000000000000000000, 0.000000000000000000, 0.000000000000000000 ) ) ;
#5134=EDGE_CURVE ( 'NONE', #11791, #2882, #7512, .T. ) ;
#5152=EDGE_CURVE ( 'NONE', #422, #15868, #3893, .T. ) ;
#5173=EDGE_CURVE ( 'NONE', #11003, #949, #53, .T. ) ;
#5280=LINE ( 'NONE', #18418, #16583 ) ;
#5307=PRESENTATION_STYLE_ASSIGNMENT (( #23658 ) ) ;
#5346=DIRECTION ( 'NONE',  ( 0.000000000000000000, 0.000000000000000000, 1.000000000000000000 ) ) ;
#5365=AXIS2_PLACEMENT_3D ( 'NONE', #12085, #8536, #21325 ) ;
#5367=ADVANCED_FACE ( 'NONE', ( #14061 ), #12257, .T. ) ;
#5382=AXIS2_PLACEMENT_3D ( 'NONE', #14177, #15428, #12622 ) ;
#5502=FACE_OUTER_BOUND ( 'NONE', #10010, .T. ) ;
#5568=AXIS2_PLACEMENT_3D ( 'NONE', #7317, #11572, #16487 ) ;
#5589=CARTESIAN_POINT ( 'NONE',  ( 2.500000000000002220, 1.178949249685212086, -2.042000000000002036 ) ) ;
#5665=VECTOR ( 'NONE', #19072, 1000.000000000000114 ) ;
#5690=ORIENTED_EDGE ( 'NONE', *, *, #8316, .T. ) ;
#5736=CIRCLE ( 'NONE', #4199, 2.041999999999999815 ) ;
#5748=CARTESIAN_POINT ( 'NONE',  ( 2.500000000000002220, 3.469446951953614189E-15, 2.041999999999998483 ) ) ;
#5767=VECTOR ( 'NONE', #8891, 1000.000000000000000 ) ;
#5807=EDGE_CURVE ( 'NONE', #22213, #11691, #15841, .T. ) ;
#5895=EDGE_CURVE ( 'NONE', #11791, #9794, #3359, .T. ) ;
#5920=DIRECTION ( 'NONE',  ( 1.000000000000000000, 0.000000000000000000, 0.000000000000000000 ) ) ;
#5928=ORIENTED_EDGE ( 'NONE', *, *, #14515, .F. ) ;
#5979=DIRECTION ( 'NONE',  ( -1.000000000000000000, 0.000000000000000000, 0.000000000000000000 ) ) ;
#6058=( NAMED_UNIT ( * ) PLANE_ANGLE_UNIT ( ) SI_UNIT ( $, .RADIAN. ) );
#6074=ORIENTED_EDGE ( 'NONE', *, *, #13128, .F. ) ;
#6084=DIRECTION ( 'NONE',  ( -1.000000000000000000, 0.000000000000000000, 0.000000000000000000 ) ) ;
#6123=CARTESIAN_POINT ( 'NONE',  ( 2.500000000000002220, 0.000000000000000000, 0.000000000000000000 ) ) ;
#6132=CARTESIAN_POINT ( 'NONE',  ( 2.500000000000002220, -1.178949249685215417, 2.042000000000002036 ) ) ;
#6152=ORIENTED_EDGE ( 'NONE', *, *, #18179, .F. ) ;
#6174=LINE ( 'NONE', #13698, #5665 ) ;
#6216=DIRECTION ( 'NONE',  ( 0.000000000000000000, 0.000000000000000000, 1.000000000000000000 ) ) ;
#6235=FACE_OUTER_BOUND ( 'NONE', #2768, .T. ) ;
#6333=AXIS2_PLACEMENT_3D ( 'NONE', #23472, #10839, #14339 ) ;
#6340=EDGE_CURVE ( 'NONE', #9973, #10543, #3457, .T. ) ;
#6425=EDGE_LOOP ( 'NONE', ( #6744, #9086, #7475, #10173, #12108 ) ) ;
#6491=DIRECTION ( 'NONE',  ( 0.000000000000000000, 0.000000000000000000, 1.000000000000000000 ) ) ;
#6508=SHAPE_REPRESENTATION ( 'socket head cap screw_iso_ISO 4762 M5 x 25 - 25N', ( #11210 ), #16951 ) ;
#6515=AXIS2_PLACEMENT_3D ( 'NONE', #4406, #5979, #11329 ) ;
#6534=STYLED_ITEM ( 'NONE', ( #5307 ), #16222 ) ;
#6577=CARTESIAN_POINT ( 'NONE',  ( 2.500000000000002220, 2.357898499370434386, -3.469446951953614189E-15 ) ) ;
#6583=VERTEX_POINT ( 'NONE', #19699 ) ;
#6597=ORIENTED_EDGE ( 'NONE', *, *, #15972, .F. ) ;
#6665=EDGE_CURVE ( 'NONE', #12522, #18989, #8475, .T. ) ;
#6680=DIRECTION ( 'NONE',  ( 0.000000000000000000, 0.000000000000000000, 1.000000000000000000 ) ) ;
#6687=DIRECTION ( 'NONE',  ( 0.000000000000000000, -1.224646799147353454E-16, 1.000000000000000000 ) ) ;
#6701=LINE ( 'NONE', #4886, #7887 ) ;
#6733=FACE_OUTER_BOUND ( 'NONE', #12712, .T. ) ;
#6744=ORIENTED_EDGE ( 'NONE', *, *, #18179, .T. ) ;
#6797=ADVANCED_FACE ( 'NONE', ( #14758 ), #19933, .F. ) ;
#6823=ORIENTED_EDGE ( 'NONE', *, *, #3960, .T. ) ;
#6830=EDGE_CURVE ( 'NONE', #3824, #11791, #15128, .T. ) ;
#6847=CIRCLE ( 'NONE', #17267, 2.055000000000000160 ) ;
#6884=ADVANCED_FACE ( 'NONE', ( #12830 ), #7345, .T. ) ;
#6889=VERTEX_POINT ( 'NONE', #7700 ) ;
#6900=DIRECTION ( 'NONE',  ( 0.000000000000000000, 0.000000000000000000, -1.000000000000000000 ) ) ;
#6968=DIRECTION ( 'NONE',  ( 0.000000000000000000, 0.000000000000000000, 1.000000000000000000 ) ) ;
#7032=ORIENTED_EDGE ( 'NONE', *, *, #19897, .T. ) ;
#7039=DIRECTION ( 'NONE',  ( 1.000000000000000000, -0.000000000000000000, -0.000000000000000000 ) ) ;
#7081=FACE_OUTER_BOUND ( 'NONE', #1382, .T. ) ;
#7178=ORIENTED_EDGE ( 'NONE', *, *, #6830, .F. ) ;
#7201=ORIENTED_EDGE ( 'NONE', *, *, #2066, .T. ) ;
#7219=DIRECTION ( 'NONE',  ( 0.000000000000000000, 1.000000000000000000, -1.103561164596346103E-15 ) ) ;
#7233=DIRECTION ( 'NONE',  ( -1.000000000000000000, 0.000000000000000000, 0.000000000000000000 ) ) ;
#7317=CARTESIAN_POINT ( 'NONE',  ( 5.200000000000020606, 0.000000000000000000, -2.700000000000007727 ) ) ;
#7341=CARTESIAN_POINT ( 'NONE',  ( 30.00000000000000000, 0.000000000000000000, -6.938893903907228378E-15 ) ) ;
#7345=CYLINDRICAL_SURFACE ( 'NONE', #12487, 4.250000000000000000 ) ;
#7347=EDGE_LOOP ( 'NONE', ( #8413, #21734 ) ) ;
#7468=UNCERTAINTY_MEASURE_WITH_UNIT (LENGTH_MEASURE( 1.000000000000000082E-05 ), #10286, 'distance_accuracy_value', 'NONE');
#7475=ORIENTED_EDGE ( 'NONE', *, *, #4358, .F. ) ;
#7492=FACE_OUTER_BOUND ( 'NONE', #1954, .T. ) ;
#7512=LINE ( 'NONE', #9104, #14509 ) ;
#7534=AXIS2_PLACEMENT_3D ( 'NONE', #8879, #3060, #8629 ) ;
#7536=LINE ( 'NONE', #17206, #1010 ) ;
#7585=ORIENTED_EDGE ( 'NONE', *, *, #23704, .F. ) ;
#7588=ADVANCED_FACE ( 'NONE', ( #6733 ), #15925, .F. ) ;
#7689=AXIS2_PLACEMENT_3D ( 'NONE', #10575, #8746, #16111 ) ;
#7694=CARTESIAN_POINT ( 'NONE',  ( 2.500000000000002220, 2.500728763858895382E-16, -2.041999999999999815 ) ) ;
#7700=CARTESIAN_POINT ( 'NONE',  ( 2.500000000000002220, 1.178949249685218970, 2.041999999999998483 ) ) ;
#7722=ORIENTED_EDGE ( 'NONE', *, *, #22406, .T. ) ;
#7727=EDGE_LOOP ( 'NONE', ( #12026, #11175 ) ) ;
#7730=CARTESIAN_POINT ( 'NONE',  ( 2.500000000000002220, 0.000000000000000000, 2.041999999999999815 ) ) ;
#7808=ADVANCED_FACE ( 'NONE', ( #6235 ), #3954, .F. ) ;
#7812=DIRECTION ( 'NONE',  ( 0.000000000000000000, 0.000000000000000000, -1.000000000000000000 ) ) ;
#7873=ORIENTED_EDGE ( 'NONE', *, *, #623, .T. ) ;
#7878=DIRECTION ( 'NONE',  ( 0.000000000000000000, 0.000000000000000000, 1.000000000000000000 ) ) ;
#7887=VECTOR ( 'NONE', #21423, 1000.000000000000114 ) ;
#7931=CARTESIAN_POINT ( 'NONE',  ( 0.2500000000000002220, 0.000000000000000000, 2.081668171172168513E-14 ) ) ;
#8001=ORIENTED_EDGE ( 'NONE', *, *, #16781, .F. ) ;
#8149=CARTESIAN_POINT ( 'NONE',  ( 2.500000000000015987, 1.768423874527823347, -1.021000000000001018 ) ) ;
#8194=ORIENTED_EDGE ( 'NONE', *, *, #18134, .F. ) ;
#8202=DIRECTION ( 'NONE',  ( 1.000000000000000000, 0.000000000000000000, 0.000000000000000000 ) ) ;
#8287=AXIS2_PLACEMENT_3D ( 'NONE', #21056, #17329, #6687 ) ;
#8295=CARTESIAN_POINT ( 'NONE',  ( 2.500000000000002220, -1.178949249685215417, 2.042000000000002036 ) ) ;
#8316=EDGE_CURVE ( 'NONE', #11691, #6889, #6174, .T. ) ;
#8413=ORIENTED_EDGE ( 'NONE', *, *, #8714, .T. ) ;
#8414=LINE ( 'NONE', #4911, #13368 ) ;
#8444=EDGE_CURVE ( 'NONE', #11003, #1963, #23553, .T. ) ;
#8475=CIRCLE ( 'NONE', #5382, 0.2000000000000000944 ) ;
#8478=CARTESIAN_POINT ( 'NONE',  ( 2.500000000000002220, 2.357898499370434386, -3.469446951953614189E-15 ) ) ;
#8519=CARTESIAN_POINT ( 'NONE',  ( 5.000000000000018652, 3.306546357697858171E-16, 2.699999999999997069 ) ) ;
#8536=DIRECTION ( 'NONE',  ( 0.000000000000000000, 0.8660254037844391517, 0.4999999999999991673 ) ) ;
#8540=DIRECTION ( 'NONE',  ( -1.000000000000000000, 0.000000000000000000, 0.000000000000000000 ) ) ;
#8620=AXIS2_PLACEMENT_3D ( 'NONE', #18644, #13529, #16994 ) ;
#8623=LINE ( 'NONE', #22008, #10005 ) ;
#8629=DIRECTION ( 'NONE',  ( 0.000000000000000000, 0.000000000000000000, 1.000000000000000000 ) ) ;
#8636=DIRECTION ( 'NONE',  ( -1.000000000000000000, 0.000000000000000000, 0.000000000000000000 ) ) ;
#8643=ORIENTED_EDGE ( 'NONE', *, *, #22012, .F. ) ;
#8673=DIRECTION ( 'NONE',  ( 1.000000000000000000, 0.000000000000000000, 0.000000000000000000 ) ) ;
#8709=AXIS2_PLACEMENT_3D ( 'NONE', #2761, #22913, #19660 ) ;
#8714=EDGE_CURVE ( 'NONE', #22000, #22474, #10731, .T. ) ;
#8746=DIRECTION ( 'NONE',  ( -1.000000000000000000, 0.000000000000000000, 0.000000000000000000 ) ) ;
#8754=ADVANCED_FACE ( 'NONE', ( #17486 ), #18783, .F. ) ;
#8755=ORIENTED_EDGE ( 'NONE', *, *, #6830, .T. ) ;
#8805=FACE_OUTER_BOUND ( 'NONE', #2556, .T. ) ;
#8822=AXIS2_PLACEMENT_3D ( 'NONE', #3208, #22696, #10620 ) ;
#8879=CARTESIAN_POINT ( 'NONE',  ( 0.2500000000000002220, 0.000000000000000000, 2.081668171172168513E-14 ) ) ;
#8891=DIRECTION ( 'NONE',  ( -1.000000000000000000, 0.000000000000000000, 0.000000000000000000 ) ) ;
#8943=CARTESIAN_POINT ( 'NONE',  ( 29.55500000000002458, 0.000000000000000000, -6.938893903907228378E-15 ) ) ;
#8959=DIRECTION ( 'NONE',  ( 0.000000000000000000, -1.287488025362403787E-15, -1.000000000000000000 ) ) ;
#8990=DIRECTION ( 'NONE',  ( 0.000000000000000000, -1.000000000000000000, 1.287488025362403787E-15 ) ) ;
#9071=LINE ( 'NONE', #3261, #18675 ) ;
#9086=ORIENTED_EDGE ( 'NONE', *, *, #10036, .F. ) ;
#9104=CARTESIAN_POINT ( 'NONE',  ( 0.000000000000000000, -1.178949249685215417, 2.042000000000002036 ) ) ;
#9108=CARTESIAN_POINT ( 'NONE',  ( 2.500000000000002220, 0.000000000000000000, 0.000000000000000000 ) ) ;
#9129=ORIENTED_EDGE ( 'NONE', *, *, #10251, .T. ) ;
#9167=VECTOR ( 'NONE', #23256, 1000.000000000000000 ) ;
#9189=PLANE ( 'NONE',  #16054 ) ;
#9244=ORIENTED_EDGE ( 'NONE', *, *, #22868, .F. ) ;
#9263=ORIENTED_EDGE ( 'NONE', *, *, #2409, .F. ) ;
#9287=ADVANCED_FACE ( 'NONE', ( #19489 ), #2942, .T. ) ;
#9366=AXIS2_PLACEMENT_3D ( 'NONE', #15808, #8202, #15575 ) ;
#9372=CARTESIAN_POINT ( 'NONE',  ( 2.500000000000002220, 1.178949249685212086, -2.042000000000002036 ) ) ;
#9422=ORIENTED_EDGE ( 'NONE', *, *, #17644, .T. ) ;
#9429=ORIENTED_EDGE ( 'NONE', *, *, #20155, .F. ) ;
#9441=CARTESIAN_POINT ( 'NONE',  ( 2.500000000000002220, 2.357898499370434386, -3.469446951953614189E-15 ) ) ;
#9460=DIRECTION ( 'NONE',  ( -1.000000000000000000, 0.000000000000000000, 0.000000000000000000 ) ) ;
#9473=CARTESIAN_POINT ( 'NONE',  ( 0.000000000000000000, 0.000000000000000000, 0.000000000000000000 ) ) ;
#9510=DIRECTION ( 'NONE',  ( -1.000000000000000000, -0.000000000000000000, -0.000000000000000000 ) ) ;
#9574=CIRCLE ( 'NONE', #11150, 2.041999999999999815 ) ;
#9575=( LENGTH_UNIT ( ) NAMED_UNIT ( * ) SI_UNIT ( .MILLI., .METRE. ) );
#9578=VECTOR ( 'NONE', #13865, 1000.000000000000000 ) ;
#9580=AXIS2_PLACEMENT_3D ( 'NONE', #7931, #19142, #13536 ) ;
#9582=ORIENTED_EDGE ( 'NONE', *, *, #19903, .F. ) ;
#9619=CIRCLE ( 'NONE', #3821, 2.700000000000000622 ) ;
#9683=DIRECTION ( 'NONE',  ( -1.000000000000000000, 0.000000000000000000, 0.000000000000000000 ) ) ;
#9754=DIRECTION ( 'NONE',  ( 0.000000000000000000, -0.5000000000000011102, -0.8660254037844379305 ) ) ;
#9764=EDGE_LOOP ( 'NONE', ( #18006, #8001, #14614 ) ) ;
#9794=VERTEX_POINT ( 'NONE', #43 ) ;
#9831=CIRCLE ( 'NONE', #5568, 0.2000000000000000944 ) ;
#9889=CARTESIAN_POINT ( 'NONE',  ( 0.000000000000000000, -2.357898499370430834, 3.469446951953614189E-15 ) ) ;
#9890=FACE_OUTER_BOUND ( 'NONE', #23544, .T. ) ;
#9937=CARTESIAN_POINT ( 'NONE',  ( 5.200000000000020606, 0.000000000000000000, -6.938893903907228378E-15 ) ) ;
#9973=VERTEX_POINT ( 'NONE', #18091 ) ;
#10005=VECTOR ( 'NONE', #12770, 1000.000000000000000 ) ;
#10010=EDGE_LOOP ( 'NONE', ( #3008, #9244, #16197 ) ) ;
#10013=AXIS2_PLACEMENT_3D ( 'NONE', #18025, #1357, #6680 ) ;
#10036=EDGE_CURVE ( 'NONE', #10801, #6583, #17603, .T. ) ;
#10048=CARTESIAN_POINT ( 'NONE',  ( 2.500000000000002220, -1.768423874527823347, 1.021000000000001018 ) ) ;
#10063=AXIS2_PLACEMENT_3D ( 'NONE', #11834, #9510, #7812 ) ;
#10125=CARTESIAN_POINT ( 'NONE',  ( 2.500000000000002220, 0.000000000000000000, 0.000000000000000000 ) ) ;
#10162=ORIENTED_EDGE ( 'NONE', *, *, #1758, .T. ) ;
#10173=ORIENTED_EDGE ( 'NONE', *, *, #5173, .F. ) ;
#10215=TOROIDAL_SURFACE ( 'NONE', #17516, 2.700000000000000622, 0.2000000000000000111 ) ;
#10221=EDGE_CURVE ( 'NONE', #15468, #11003, #22780, .T. ) ;
#10246=PLANE ( 'NONE',  #11375 ) ;
#10251=EDGE_CURVE ( 'NONE', #18989, #19049, #5033, .T. ) ;
#10271=CARTESIAN_POINT ( 'NONE',  ( 2.500000000000002220, -1.178949249685215417, 2.042000000000002036 ) ) ;
#10286=( LENGTH_UNIT ( ) NAMED_UNIT ( * ) SI_UNIT ( .MILLI., .METRE. ) );
#10436=ORIENTED_EDGE ( 'NONE', *, *, #1554, .T. ) ;
#10470=FACE_OUTER_BOUND ( 'NONE', #19124, .T. ) ;
#10494=DIRECTION ( 'NONE',  ( 0.000000000000000000, -0.5000000000000011102, -0.8660254037844379305 ) ) ;
#10503=ADVANCED_FACE ( 'NONE', ( #22997 ), #13998, .T. ) ;
#10520=CYLINDRICAL_SURFACE ( 'NONE', #8709, 4.250000000000000000 ) ;
#10543=VERTEX_POINT ( 'NONE', #21901 ) ;
#10566=CARTESIAN_POINT ( 'NONE',  ( 0.2500000000000002220, 0.000000000000000000, 4.000000000000021316 ) ) ;
#10575=CARTESIAN_POINT ( 'NONE',  ( 0.000000000000000000, 0.000000000000000000, 0.000000000000000000 ) ) ;
#10591=CARTESIAN_POINT ( 'NONE',  ( 29.55500000000002458, 0.000000000000000000, -6.938893903907228378E-15 ) ) ;
#10617=DIRECTION ( 'NONE',  ( 0.000000000000000000, 0.4999999999999991118, -0.8660254037844391517 ) ) ;
#10620=DIRECTION ( 'NONE',  ( 0.000000000000000000, 0.4999999999999992784, -0.8660254037844390407 ) ) ;
#10640=VECTOR ( 'NONE', #21475, 1000.000000000000000 ) ;
#10665=ORIENTED_EDGE ( 'NONE', *, *, #5807, .F. ) ;
#10691=DIRECTION ( 'NONE',  ( 0.000000000000000000, -0.5000000000000009992, -0.8660254037844380415 ) ) ;
#10728=DIRECTION ( 'NONE',  ( -1.000000000000000000, 0.000000000000000000, 0.000000000000000000 ) ) ;
#10731=CIRCLE ( 'NONE', #14558, 4.000000000000000000 ) ;
#10737=CIRCLE ( 'NONE', #1062, 4.250000000000000000 ) ;
#10751=CARTESIAN_POINT ( 'NONE',  ( 5.200000000000020606, 0.000000000000000000, -6.938893903907228378E-15 ) ) ;
#10792=STYLED_ITEM('',(#23927),#4076);
#10801=VERTEX_POINT ( 'NONE', #23095 ) ;
#10835=DIRECTION ( 'NONE',  ( -1.000000000000000000, 0.000000000000000000, 0.000000000000000000 ) ) ;
#10839=DIRECTION ( 'NONE',  ( -1.000000000000000000, 0.000000000000000000, 0.000000000000000000 ) ) ;
#10841=AXIS2_PLACEMENT_3D ( 'NONE', #10566, #17658, #1122 ) ;
#10847=EDGE_LOOP ( 'NONE', ( #11897, #14795, #1416, #16051 ) ) ;
#10863=CARTESIAN_POINT ( 'NONE',  ( 5.000000000000015099, 0.000000000000000000, 0.000000000000000000 ) ) ;
#10963=CONICAL_SURFACE ( 'NONE', #13691, 2.041999999999999815, 1.047197551196591858 ) ;
#11003=VERTEX_POINT ( 'NONE', #9372 ) ;
#11009=CIRCLE ( 'NONE', #17513, 2.041999999999999815 ) ;
#11115=DIRECTION ( 'NONE',  ( -1.000000000000000000, 0.000000000000000000, 0.000000000000000000 ) ) ;
#11146=ORIENTED_EDGE ( 'NONE', *, *, #21854, .F. ) ;
#11150=AXIS2_PLACEMENT_3D ( 'NONE', #10125, #8540, #17580 ) ;
#11175=ORIENTED_EDGE ( 'NONE', *, *, #17644, .F. ) ;
#11210=AXIS2_PLACEMENT_3D ( 'NONE', #9473, #14914, #3769 ) ;
#11212=AXIS2_PLACEMENT_3D ( 'NONE', #13830, #21154, #6900 ) ;
#11222=PLANE ( 'NONE',  #3758 ) ;
#11238=CARTESIAN_POINT ( 'NONE',  ( 0.000000000000000000, 2.357898499370434386, -3.469446951953614189E-15 ) ) ;
#11239=DIRECTION ( 'NONE',  ( 0.000000000000000000, 0.000000000000000000, -1.000000000000000000 ) ) ;
#11251=ORIENTED_EDGE ( 'NONE', *, *, #5173, .T. ) ;
#11260=ORIENTED_EDGE ( 'NONE', *, *, #12126, .T. ) ;
#11301=EDGE_LOOP ( 'NONE', ( #5024, #3714, #15495, #4061, #6152, #15042 ) ) ;
#11302=DIRECTION ( 'NONE',  ( -1.000000000000000000, 0.000000000000000000, 0.000000000000000000 ) ) ;
#11310=ORIENTED_EDGE ( 'NONE', *, *, #3276, .T. ) ;
#11329=DIRECTION ( 'NONE',  ( 0.000000000000000000, 0.000000000000000000, 1.000000000000000000 ) ) ;
#11362=VECTOR ( 'NONE', #18640, 1000.000000000000000 ) ;
#11375=AXIS2_PLACEMENT_3D ( 'NONE', #6132, #17587, #922 ) ;
#11443=EDGE_CURVE ( 'NONE', #949, #10543, #14054, .T. ) ;
#11454=( NAMED_UNIT ( * ) PLANE_ANGLE_UNIT ( ) SI_UNIT ( $, .RADIAN. ) );
#11478=VECTOR ( 'NONE', #10691, 1000.000000000000114 ) ;
#11572=DIRECTION ( 'NONE',  ( 0.000000000000000000, -1.000000000000000000, 0.000000000000000000 ) ) ;
#11584=VERTEX_POINT ( 'NONE', #10048 ) ;
#11627=FACE_OUTER_BOUND ( 'NONE', #18043, .T. ) ;
#11632=LINE ( 'NONE', #7730, #19159 ) ;
#11659=CARTESIAN_POINT ( 'NONE',  ( 2.500000000000002220, -3.469446951953614189E-15, -2.041999999999998483 ) ) ;
#11691=VERTEX_POINT ( 'NONE', #19668 ) ;
#11743=ORIENTED_EDGE ( 'NONE', *, *, #3209, .T. ) ;
#11791=VERTEX_POINT ( 'NONE', #14491 ) ;
#11823=ADVANCED_FACE ( 'NONE', ( #3702 ), #10963, .F. ) ;
#11834=CARTESIAN_POINT ( 'NONE',  ( 5.000000000000015099, 0.000000000000000000, 0.000000000000000000 ) ) ;
#11864=CARTESIAN_POINT ( 'NONE',  ( 2.500000000000002220, 2.357898499370434386, -3.469446951953614189E-15 ) ) ;
#11871=AXIS2_PLACEMENT_3D ( 'NONE', #9937, #20907, #11890 ) ;
#11890=DIRECTION ( 'NONE',  ( 0.000000000000000000, 0.000000000000000000, -1.000000000000000000 ) ) ;
#11897=ORIENTED_EDGE ( 'NONE', *, *, #17558, .T. ) ;
#11964=ADVANCED_FACE ( 'NONE', ( #9890 ), #10246, .T. ) ;
#11997=ORIENTED_EDGE ( 'NONE', *, *, #5134, .F. ) ;
#12026=ORIENTED_EDGE ( 'NONE', *, *, #17558, .F. ) ;
#12075=CARTESIAN_POINT ( 'NONE',  ( 3.678949249685231848, 0.000000000000000000, -6.938893903907228378E-15 ) ) ;
#12085=CARTESIAN_POINT ( 'NONE',  ( 2.500000000000002220, -2.357898499370430834, 3.469446951953614189E-15 ) ) ;
#12108=ORIENTED_EDGE ( 'NONE', *, *, #8444, .T. ) ;
#12126=EDGE_CURVE ( 'NONE', #23349, #19049, #9831, .T. ) ;
#12178=CARTESIAN_POINT ( 'NONE',  ( 0.000000000000000000, 5.051668046482844583E-16, -4.000000000000000000 ) ) ;
#12194=EDGE_CURVE ( 'NONE', #3824, #22213, #1743, .T. ) ;
#12257=PLANE ( 'NONE',  #11212 ) ;
#12320=DIRECTION ( 'NONE',  ( 0.000000000000000000, -0.4999999999999992228, 0.8660254037844390407 ) ) ;
#12350=ORIENTED_EDGE ( 'NONE', *, *, #20155, .T. ) ;
#12373=ORIENTED_EDGE ( 'NONE', *, *, #17140, .T. ) ;
#12430=CARTESIAN_POINT ( 'NONE',  ( 29.55500000000002458, 0.000000000000000000, 2.499999999999987121 ) ) ;
#12446=CARTESIAN_POINT ( 'NONE',  ( 0.000000000000000000, 1.178949249685212086, -2.042000000000002036 ) ) ;
#12487=AXIS2_PLACEMENT_3D ( 'NONE', #18317, #16517, #1769 ) ;
#12504=VERTEX_POINT ( 'NONE', #15385 ) ;
#12522=VERTEX_POINT ( 'NONE', #525 ) ;
#12545=ORIENTED_EDGE ( 'NONE', *, *, #11443, .T. ) ;
#12592=ORIENTED_EDGE ( 'NONE', *, *, #3276, .F. ) ;
#12601=LINE ( 'NONE', #23550, #17302 ) ;
#12622=DIRECTION ( 'NONE',  ( 0.000000000000000000, 1.224646799147353207E-16, 1.000000000000000000 ) ) ;
#12712=EDGE_LOOP ( 'NONE', ( #3927, #15665, #10665 ) ) ;
#12733=PRODUCT ( 'socket head cap screw_iso_ISO 4762 M5 x 25 - 25N', 'socket head cap screw_iso_ISO 4762 M5 x 25 - 25N', '', ( #15100 ) ) ;
#12770=DIRECTION ( 'NONE',  ( -1.000000000000000000, 0.000000000000000000, 0.000000000000000000 ) ) ;
#12830=FACE_OUTER_BOUND ( 'NONE', #13683, .T. ) ;
#12845=UNCERTAINTY_MEASURE_WITH_UNIT (LENGTH_MEASURE( 1.000000000000000082E-05 ), #17994, 'distance_accuracy_value', 'NONE');
#12852=CARTESIAN_POINT ( 'NONE',  ( 5.000000000000015099, 0.000000000000000000, 4.250000000000000000 ) ) ;
#13032=EDGE_CURVE ( 'NONE', #23797, #12522, #16630, .T. ) ;
#13035=CARTESIAN_POINT ( 'NONE',  ( -31.74999999999994316, 0.000000000000000000, 2.500000000000000444 ) ) ;
#13128=EDGE_CURVE ( 'NONE', #11691, #15468, #11009, .T. ) ;
#13191=DIRECTION ( 'NONE',  ( 0.000000000000000000, 0.000000000000000000, 1.000000000000000000 ) ) ;
#13211=ADVANCED_FACE ( 'NONE', ( #3071 ), #20209, .T. ) ;
#13335=EDGE_CURVE ( 'NONE', #4538, #23797, #6701, .T. ) ;
#13368=VECTOR ( 'NONE', #12320, 1000.000000000000114 ) ;
#13424=ORIENTED_EDGE ( 'NONE', *, *, #16963, .T. ) ;
#13436=LINE ( 'NONE', #10271, #10640 ) ;
#13450=DIRECTION ( 'NONE',  ( 0.000000000000000000, 0.000000000000000000, -1.000000000000000000 ) ) ;
#13509=VERTEX_POINT ( 'NONE', #2560 ) ;
#13529=DIRECTION ( 'NONE',  ( -1.000000000000000000, 0.000000000000000000, 0.000000000000000000 ) ) ;
#13536=DIRECTION ( 'NONE',  ( 0.000000000000000000, 0.000000000000000000, 1.000000000000000000 ) ) ;
#13585=PLANE ( 'NONE',  #18448 ) ;
#13683=EDGE_LOOP ( 'NONE', ( #7585, #22369, #7722, #4700 ) ) ;
#13691=AXIS2_PLACEMENT_3D ( 'NONE', #14848, #22179, #13191 ) ;
#13698=CARTESIAN_POINT ( 'NONE',  ( 2.500000000000002220, 2.357898499370434386, -3.469446951953614189E-15 ) ) ;
#13830=CARTESIAN_POINT ( 'NONE',  ( 30.00000000000000000, 2.054999999999997939, -6.938893903907228378E-15 ) ) ;
#13865=DIRECTION ( 'NONE',  ( -1.000000000000000000, 0.000000000000000000, 0.000000000000000000 ) ) ;
#13912=VECTOR ( 'NONE', #10617, 1000.000000000000000 ) ;
#13942=CARTESIAN_POINT ( 'NONE',  ( 2.500000000000002220, 1.178949249685212086, -2.042000000000002036 ) ) ;
#13989=CARTESIAN_POINT ( 'NONE',  ( 2.500000000000002220, 0.000000000000000000, 0.000000000000000000 ) ) ;
#13998=PLANE ( 'NONE',  #5365 ) ;
#14000=FACE_OUTER_BOUND ( 'NONE', #23195, .T. ) ;
#14012=DIRECTION ( 'NONE',  ( 0.000000000000000000, 0.000000000000000000, -1.000000000000000000 ) ) ;
#14054=CIRCLE ( 'NONE', #914, 2.041999999999999815 ) ;
#14061=FACE_OUTER_BOUND ( 'NONE', #7727, .T. ) ;
#14134=CARTESIAN_POINT ( 'NONE',  ( 5.200000000000020606, 0.000000000000000000, -6.938893903907228378E-15 ) ) ;
#14144=ORIENTED_EDGE ( 'NONE', *, *, #3960, .F. ) ;
#14177=CARTESIAN_POINT ( 'NONE',  ( 5.200000000000020606, 3.306546357697854226E-16, 2.699999999999993516 ) ) ;
#14239=AXIS2_PLACEMENT_3D ( 'NONE', #6123, #20720, #15449 ) ;
#14280=( GEOMETRIC_REPRESENTATION_CONTEXT ( 3 ) GLOBAL_UNCERTAINTY_ASSIGNED_CONTEXT ( ( #12845 ) ) GLOBAL_UNIT_ASSIGNED_CONTEXT ( ( #17994, #11454, #20477 ) ) REPRESENTATION_CONTEXT ( 'NONE', 'WORKASPACE' ) );
#14339=DIRECTION ( 'NONE',  ( 0.000000000000000000, 0.000000000000000000, 1.000000000000000000 ) ) ;
#14400=SHAPE_REPRESENTATION_RELATIONSHIP ( 'NONE' , 'NONE' ,  #6508, #16222 ) ;
#14468=DIRECTION ( 'NONE',  ( 0.000000000000000000, 0.000000000000000000, -1.000000000000000000 ) ) ;
#14491=CARTESIAN_POINT ( 'NONE',  ( 0.000000000000000000, -1.178949249685215417, 2.042000000000002036 ) ) ;
#14504=( NAMED_UNIT ( * ) SI_UNIT ( $, .STERADIAN. ) SOLID_ANGLE_UNIT ( ) );
#14509=VECTOR ( 'NONE', #2072, 1000.000000000000114 ) ;
#14515=EDGE_CURVE ( 'NONE', #422, #15468, #15912, .T. ) ;
#14539=EDGE_CURVE ( 'NONE', #9973, #2882, #17728, .T. ) ;
#14558=AXIS2_PLACEMENT_3D ( 'NONE', #15813, #17966, #6491 ) ;
#14614=ORIENTED_EDGE ( 'NONE', *, *, #1758, .F. ) ;
#14665=FACE_BOUND ( 'NONE', #11301, .T. ) ;
#14708=DIRECTION ( 'NONE',  ( 1.000000000000000000, 0.000000000000000000, 0.000000000000000000 ) ) ;
#14749=CARTESIAN_POINT ( 'NONE',  ( 2.500000000000002220, 1.178949249685212086, -2.042000000000002036 ) ) ;
#14758=FACE_OUTER_BOUND ( 'NONE', #9764, .T. ) ;
#14762=EDGE_CURVE ( 'NONE', #6889, #9794, #5280, .T. ) ;
#14795=ORIENTED_EDGE ( 'NONE', *, *, #2411, .T. ) ;
#14848=CARTESIAN_POINT ( 'NONE',  ( 2.500000000000002220, 0.000000000000000000, 0.000000000000000000 ) ) ;
#14910=DIRECTION ( 'NONE',  ( 0.000000000000000000, 0.000000000000000000, -1.000000000000000000 ) ) ;
#14914=DIRECTION ( 'NONE',  ( 0.000000000000000000, 0.000000000000000000, 1.000000000000000000 ) ) ;
#15003=EDGE_LOOP ( 'NONE', ( #19303, #16860, #14144, #969 ) ) ;
#15042=ORIENTED_EDGE ( 'NONE', *, *, #19897, .F. ) ;
#15064=CARTESIAN_POINT ( 'NONE',  ( 2.500000000000002220, -1.178949249685215417, 2.042000000000002036 ) ) ;
#15085=DIRECTION ( 'NONE',  ( -0.5000000000000051070, 1.060575238724903217E-16, -0.8660254037844355990 ) ) ;
#15100=PRODUCT_CONTEXT ( 'NONE', #15572, 'mechanical' ) ;
#15128=LINE ( 'NONE', #20641, #4716 ) ;
#15270=CLOSED_SHELL ( 'NONE', ( #7808, #4995, #8754, #322, #18206, #3349, #2514, #5367, #17101, #9287, #20952, #6884, #510, #13211, #20696, #705, #11964, #10503, #1242, #21809, #22216, #6797, #22607, #7588, #3823, #20817, #11823 ) ) ;
#15336=CARTESIAN_POINT ( 'NONE',  ( -31.74999999999994316, 0.000000000000000000, 0.000000000000000000 ) ) ;
#15385=CARTESIAN_POINT ( 'NONE',  ( 0.2500000000000002220, 0.000000000000000000, 4.250000000000021316 ) ) ;
#15395=AXIS2_PLACEMENT_3D ( 'NONE', #3676, #14708, #14468 ) ;
#15428=DIRECTION ( 'NONE',  ( 0.000000000000000000, 1.000000000000000000, -1.224646799147353207E-16 ) ) ;
#15446=DIRECTION ( 'NONE',  ( 0.000000000000000000, -1.000000000000000000, 1.103561164596346103E-15 ) ) ;
#15449=DIRECTION ( 'NONE',  ( 0.000000000000000000, 0.000000000000000000, 1.000000000000000000 ) ) ;
#15452=ORIENTED_EDGE ( 'NONE', *, *, #22406, .F. ) ;
#15468=VERTEX_POINT ( 'NONE', #8149 ) ;
#15495=ORIENTED_EDGE ( 'NONE', *, *, #5134, .T. ) ;
#15502=LINE ( 'NONE', #4722, #21801 ) ;
#15528=DIRECTION ( 'NONE',  ( 0.000000000000000000, 0.000000000000000000, 1.000000000000000000 ) ) ;
#15572=APPLICATION_CONTEXT ( 'automotive_design' ) ;
#15575=DIRECTION ( 'NONE',  ( 0.000000000000000000, 0.000000000000000000, -1.000000000000000000 ) ) ;
#15591=CARTESIAN_POINT ( 'NONE',  ( 5.200000000000020606, 0.000000000000000000, -6.938893903907228378E-15 ) ) ;
#15603=EDGE_LOOP ( 'NONE', ( #21499, #3552, #11310, #2600 ) ) ;
#15658=VECTOR ( 'NONE', #23194, 1000.000000000000114 ) ;
#15665=ORIENTED_EDGE ( 'NONE', *, *, #8316, .F. ) ;
#15734=AXIS2_PLACEMENT_3D ( 'NONE', #8943, #11115, #19901 ) ;
#15772=LINE ( 'NONE', #1380, #5767 ) ;
#15802=LINE ( 'NONE', #23621, #9167 ) ;
#15806=CARTESIAN_POINT ( 'NONE',  ( 2.500000000000002220, 2.357898499370434386, -3.469446951953614189E-15 ) ) ;
#15808=CARTESIAN_POINT ( 'NONE',  ( 2.500000000000002220, 2.357898499370434386, -3.469446951953614189E-15 ) ) ;
#15813=CARTESIAN_POINT ( 'NONE',  ( 0.000000000000000000, 0.000000000000000000, 0.000000000000000000 ) ) ;
#15823=DIRECTION ( 'NONE',  ( -1.000000000000000000, 0.000000000000000000, 0.000000000000000000 ) ) ;
#15824=EDGE_LOOP ( 'NONE', ( #9263, #187, #123, #13424 ) ) ;
#15841=CIRCLE ( 'NONE', #22373, 2.041999999999999815 ) ;
#15863=ORIENTED_EDGE ( 'NONE', *, *, #2241, .T. ) ;
#15868=VERTEX_POINT ( 'NONE', #11238 ) ;
#15905=EDGE_LOOP ( 'NONE', ( #18805, #9422, #4111, #11146 ) ) ;
#15912=LINE ( 'NONE', #23247, #17368 ) ;
#15923=FACE_OUTER_BOUND ( 'NONE', #21191, .T. ) ;
#15925=PLANE ( 'NONE',  #9366 ) ;
#15950=DIRECTION ( 'NONE',  ( 0.000000000000000000, 0.4999999999999991118, -0.8660254037844391517 ) ) ;
#15969=ORIENTED_EDGE ( 'NONE', *, *, #5152, .F. ) ;
#15972=EDGE_CURVE ( 'NONE', #13509, #12504, #21527, .T. ) ;
#16051=ORIENTED_EDGE ( 'NONE', *, *, #13335, .F. ) ;
#16054=AXIS2_PLACEMENT_3D ( 'NONE', #14749, #8959, #22079 ) ;
#16057=TOROIDAL_SURFACE ( 'NONE', #7534, 4.000000000000000000, 0.2500000000000000000 ) ;
#16111=DIRECTION ( 'NONE',  ( 0.000000000000000000, 0.000000000000000000, 1.000000000000000000 ) ) ;
#16112=CARTESIAN_POINT ( 'NONE',  ( 2.500000000000002220, -1.178949249685215417, 2.042000000000002036 ) ) ;
#16123=DIRECTION ( 'NONE',  ( 0.000000000000000000, 0.000000000000000000, 1.000000000000000000 ) ) ;
#16197=ORIENTED_EDGE ( 'NONE', *, *, #11443, .F. ) ;
#16222=ADVANCED_BREP_SHAPE_REPRESENTATION ( '', ( #4076, #11210 ), #16951 ) ;
#16314=SURFACE_STYLE_FILL_AREA ( #451 ) ;
#16383=PLANE ( 'NONE',  #15395 ) ;
#16425=FACE_OUTER_BOUND ( 'NONE', #15905, .T. ) ;
#16447=CIRCLE ( 'NONE', #11871, 2.500000000000000444 ) ;
#16455=CARTESIAN_POINT ( 'NONE',  ( 30.00000000000000000, 2.516649172247811061E-16, -2.055000000000006821 ) ) ;
#16456=DIRECTION ( 'NONE',  ( -1.000000000000000000, -0.000000000000000000, -0.000000000000000000 ) ) ;
#16487=DIRECTION ( 'NONE',  ( 0.000000000000000000, 0.000000000000000000, -1.000000000000000000 ) ) ;
#16517=DIRECTION ( 'NONE',  ( -1.000000000000000000, 0.000000000000000000, 0.000000000000000000 ) ) ;
#16583=VECTOR ( 'NONE', #1877, 1000.000000000000000 ) ;
#16630=LINE ( 'NONE', #13035, #11362 ) ;
#16684=DIRECTION ( 'NONE',  ( 0.000000000000000000, 0.5000000000000011102, 0.8660254037844380415 ) ) ;
#16712=CARTESIAN_POINT ( 'NONE',  ( 2.500000000000002220, 2.357898499370434386, -3.469446951953614189E-15 ) ) ;
#16737=DIRECTION ( 'NONE',  ( 0.000000000000000000, 0.000000000000000000, -1.000000000000000000 ) ) ;
#16781=EDGE_CURVE ( 'NONE', #11584, #9973, #21654, .T. ) ;
#16795=DIRECTION ( 'NONE',  ( 0.000000000000000000, 0.8660254037844380415, -0.5000000000000011102 ) ) ;
#16860=ORIENTED_EDGE ( 'NONE', *, *, #6665, .T. ) ;
#16862=CARTESIAN_POINT ( 'NONE',  ( 2.500000000000002220, 2.357898499370434386, -3.469446951953614189E-15 ) ) ;
#16875=CIRCLE ( 'NONE', #19176, 2.055000000000000160 ) ;
#16889=DIRECTION ( 'NONE',  ( 0.000000000000000000, 0.000000000000000000, 1.000000000000000000 ) ) ;
#16951=( GEOMETRIC_REPRESENTATION_CONTEXT ( 3 ) GLOBAL_UNCERTAINTY_ASSIGNED_CONTEXT ( ( #7468 ) ) GLOBAL_UNIT_ASSIGNED_CONTEXT ( ( #10286, #19918, #14504 ) ) REPRESENTATION_CONTEXT ( 'NONE', 'WORKASPACE' ) );
#16963=EDGE_CURVE ( 'NONE', #12522, #23349, #16447, .T. ) ;
#16967=CARTESIAN_POINT ( 'NONE',  ( 30.00000000000000000, 0.000000000000000000, -6.938893903907228378E-15 ) ) ;
#16993=CARTESIAN_POINT ( 'NONE',  ( 5.200000000000020606, 3.061616997868392016E-16, -2.500000000000007994 ) ) ;
#16994=DIRECTION ( 'NONE',  ( 0.000000000000000000, 0.000000000000000000, 1.000000000000000000 ) ) ;
#17018=ORIENTED_EDGE ( 'NONE', *, *, #6340, .T. ) ;
#17051=ORIENTED_EDGE ( 'NONE', *, *, #10251, .F. ) ;
#17092=VERTEX_POINT ( 'NONE', #23303 ) ;
#17101=ADVANCED_FACE ( 'NONE', ( #16425 ), #20302, .T. ) ;
#17113=LINE ( 'NONE', #7694, #4026 ) ;
#17140=EDGE_CURVE ( 'NONE', #21238, #22213, #11632, .T. ) ;
#17206=CARTESIAN_POINT ( 'NONE',  ( 2.500000000000002220, -1.178949249685215417, 2.042000000000002036 ) ) ;
#17267=AXIS2_PLACEMENT_3D ( 'NONE', #7341, #20129, #15528 ) ;
#17302=VECTOR ( 'NONE', #15950, 1000.000000000000000 ) ;
#17327=CONICAL_SURFACE ( 'NONE', #10013, 2.055000000000000160, 0.7853981633974717047 ) ;
#17329=DIRECTION ( 'NONE',  ( 0.000000000000000000, 1.000000000000000000, 1.224646799147353207E-16 ) ) ;
#17345=DIRECTION ( 'NONE',  ( 0.000000000000000000, -0.5000000000000011102, -0.8660254037844379305 ) ) ;
#17368=VECTOR ( 'NONE', #10494, 1000.000000000000114 ) ;
#17404=DIRECTION ( 'NONE',  ( 0.000000000000000000, 0.000000000000000000, 1.000000000000000000 ) ) ;
#17486=FACE_OUTER_BOUND ( 'NONE', #15003, .T. ) ;
#17513=AXIS2_PLACEMENT_3D ( 'NONE', #13989, #23118, #4768 ) ;
#17516=AXIS2_PLACEMENT_3D ( 'NONE', #10751, #18914, #11239 ) ;
#17558=EDGE_CURVE ( 'NONE', #4538, #17092, #16875, .T. ) ;
#17580=DIRECTION ( 'NONE',  ( 0.000000000000000000, 0.000000000000000000, 1.000000000000000000 ) ) ;
#17587=DIRECTION ( 'NONE',  ( 0.000000000000000000, 0.8660254037844380415, -0.5000000000000009992 ) ) ;
#17603=LINE ( 'NONE', #1056, #21235 ) ;
#17618=DIRECTION ( 'NONE',  ( -1.000000000000000000, 0.000000000000000000, 0.000000000000000000 ) ) ;
#17644=EDGE_CURVE ( 'NONE', #17092, #4538, #6847, .T. ) ;
#17652=ORIENTED_EDGE ( 'NONE', *, *, #14762, .T. ) ;
#17658=DIRECTION ( 'NONE',  ( 0.000000000000000000, -1.000000000000000000, 0.000000000000000000 ) ) ;
#17689=CARTESIAN_POINT ( 'NONE',  ( -31.74999999999994316, 0.000000000000000000, 0.000000000000000000 ) ) ;
#17699=CIRCLE ( 'NONE', #6515, 4.250000000000000000 ) ;
#17700=MECHANICAL_DESIGN_GEOMETRIC_PRESENTATION_REPRESENTATION('',(#6534),#14280);
#17728=LINE ( 'NONE', #23266, #18119 ) ;
#17808=CARTESIAN_POINT ( 'NONE',  ( 5.000000000000018652, 0.000000000000000000, -2.700000000000004174 ) ) ;
#17857=DIRECTION ( 'NONE',  ( 0.000000000000000000, 0.000000000000000000, -1.000000000000000000 ) ) ;
#17868=EDGE_CURVE ( 'NONE', #12504, #13509, #10737, .T. ) ;
#17966=DIRECTION ( 'NONE',  ( -1.000000000000000000, 0.000000000000000000, 0.000000000000000000 ) ) ;
#17994=( LENGTH_UNIT ( ) NAMED_UNIT ( * ) SI_UNIT ( .MILLI., .METRE. ) );
#18006=ORIENTED_EDGE ( 'NONE', *, *, #6340, .F. ) ;
#18025=CARTESIAN_POINT ( 'NONE',  ( 30.00000000000000000, 0.000000000000000000, -6.938893903907228378E-15 ) ) ;
#18043=EDGE_LOOP ( 'NONE', ( #3516, #2790, #10436, #22346 ) ) ;
#18091=CARTESIAN_POINT ( 'NONE',  ( 2.500000000000002220, -2.357898499370430834, 3.469446951953614189E-15 ) ) ;
#18119=VECTOR ( 'NONE', #19521, 1000.000000000000000 ) ;
#18133=CIRCLE ( 'NONE', #21156, 4.250000000000000000 ) ;
#18134=EDGE_CURVE ( 'NONE', #422, #11691, #22942, .T. ) ;
#18179=EDGE_CURVE ( 'NONE', #1963, #6583, #15502, .T. ) ;
#18206=ADVANCED_FACE ( 'NONE', ( #11627 ), #20880, .T. ) ;
#18230=ORIENTED_EDGE ( 'NONE', *, *, #13128, .T. ) ;
#18317=CARTESIAN_POINT ( 'NONE',  ( -31.74999999999994316, 0.000000000000000000, 0.000000000000000000 ) ) ;
#18343=FACE_OUTER_BOUND ( 'NONE', #6425, .T. ) ;
#18418=CARTESIAN_POINT ( 'NONE',  ( 2.500000000000002220, 1.178949249685218970, 2.041999999999998483 ) ) ;
#18448=AXIS2_PLACEMENT_3D ( 'NONE', #15806, #4349, #14012 ) ;
#18551=EDGE_CURVE ( 'NONE', #15868, #9794, #8414, .T. ) ;
#18632=ORIENTED_EDGE ( 'NONE', *, *, #623, .F. ) ;
#18640=DIRECTION ( 'NONE',  ( -1.000000000000000000, 0.000000000000000000, 0.000000000000000000 ) ) ;
#18644=CARTESIAN_POINT ( 'NONE',  ( 2.500000000000002220, 0.000000000000000000, 0.000000000000000000 ) ) ;
#18647=SURFACE_SIDE_STYLE ('',( #16314 ) ) ;
#18675=VECTOR ( 'NONE', #21982, 1000.000000000000000 ) ;
#18681=PRODUCT_DEFINITION_CONTEXT ( 'detailed design', #20934, 'design' ) ;
#18702=DIRECTION ( 'NONE',  ( -1.000000000000000000, 0.000000000000000000, 0.000000000000000000 ) ) ;
#18783=TOROIDAL_SURFACE ( 'NONE', #2593, 2.700000000000000622, 0.2000000000000000111 ) ;
#18805=ORIENTED_EDGE ( 'NONE', *, *, #2411, .F. ) ;
#18914=DIRECTION ( 'NONE',  ( 1.000000000000000000, 0.000000000000000000, 0.000000000000000000 ) ) ;
#18989=VERTEX_POINT ( 'NONE', #8519 ) ;
#19049=VERTEX_POINT ( 'NONE', #17808 ) ;
#19072=DIRECTION ( 'NONE',  ( 0.000000000000000000, -0.4999999999999992228, 0.8660254037844390407 ) ) ;
#19077=MECHANICAL_DESIGN_GEOMETRIC_PRESENTATION_REPRESENTATION('',(#10792),#588);
#19124=EDGE_LOOP ( 'NONE', ( #6597, #15863, #22961, #12592 ) ) ;
#19142=DIRECTION ( 'NONE',  ( 1.000000000000000000, -0.000000000000000000, -0.000000000000000000 ) ) ;
#19159=VECTOR ( 'NONE', #20385, 1000.000000000000114 ) ;
#19176=AXIS2_PLACEMENT_3D ( 'NONE', #16967, #6084, #6216 ) ;
#19197=PRODUCT_DEFINITION ( 'UNKNOWN', '', #2305, #18681 ) ;
#19303=ORIENTED_EDGE ( 'NONE', *, *, #16963, .F. ) ;
#19353=DIRECTION ( 'NONE',  ( 0.000000000000000000, 0.000000000000000000, -1.000000000000000000 ) ) ;
#19489=FACE_OUTER_BOUND ( 'NONE', #15824, .T. ) ;
#19521=DIRECTION ( 'NONE',  ( -1.000000000000000000, 0.000000000000000000, 0.000000000000000000 ) ) ;
#19590=FACE_OUTER_BOUND ( 'NONE', #21817, .T. ) ;
#19628=AXIS2_PLACEMENT_3D ( 'NONE', #6577, #23461, #19353 ) ;
#19660=DIRECTION ( 'NONE',  ( 0.000000000000000000, 0.000000000000000000, 1.000000000000000000 ) ) ;
#19668=CARTESIAN_POINT ( 'NONE',  ( 2.500000000000002220, 1.768423874527826678, 1.020999999999997687 ) ) ;
#19670=ORIENTED_EDGE ( 'NONE', *, *, #22868, .T. ) ;
#19699=CARTESIAN_POINT ( 'NONE',  ( 0.000000000000000000, -1.178949249685218970, -2.041999999999998483 ) ) ;
#19716=PLANE ( 'NONE',  #7689 ) ;
#19830=FACE_OUTER_BOUND ( 'NONE', #10847, .T. ) ;
#19831=CARTESIAN_POINT ( 'NONE',  ( 2.500000000000002220, -1.178949249685215417, 2.042000000000002036 ) ) ;
#19838=CIRCLE ( 'NONE', #8287, 0.2500000000000002220 ) ;
#19871=ORIENTED_EDGE ( 'NONE', *, *, #1850, .T. ) ;
#19877=CARTESIAN_POINT ( 'NONE',  ( 2.500000000000002220, -2.357898499370430834, 3.469446951953614189E-15 ) ) ;
#19897=EDGE_CURVE ( 'NONE', #15868, #1963, #22270, .T. ) ;
#19901=DIRECTION ( 'NONE',  ( 0.000000000000000000, 0.000000000000000000, 1.000000000000000000 ) ) ;
#19903=EDGE_CURVE ( 'NONE', #20959, #4361, #17699, .T. ) ;
#19918=( NAMED_UNIT ( * ) PLANE_ANGLE_UNIT ( ) SI_UNIT ( $, .RADIAN. ) );
#19924=FACE_OUTER_BOUND ( 'NONE', #1544, .T. ) ;
#19933=PLANE ( 'NONE',  #20142 ) ;
#19958=ORIENTED_EDGE ( 'NONE', *, *, #14539, .F. ) ;
#20007=VECTOR ( 'NONE', #9754, 1000.000000000000114 ) ;
#20010=ORIENTED_EDGE ( 'NONE', *, *, #17140, .F. ) ;
#20054=ORIENTED_EDGE ( 'NONE', *, *, #3209, .F. ) ;
#20129=DIRECTION ( 'NONE',  ( -1.000000000000000000, 0.000000000000000000, 0.000000000000000000 ) ) ;
#20142=AXIS2_PLACEMENT_3D ( 'NONE', #20766, #5920, #13450 ) ;
#20155=EDGE_CURVE ( 'NONE', #15468, #949, #5736, .T. ) ;
#20209=TOROIDAL_SURFACE ( 'NONE', #6333, 4.000000000000000000, 0.2500000000000000000 ) ;
#20221=CARTESIAN_POINT ( 'NONE',  ( 2.500000000000002220, 2.357898499370434386, -3.469446951953614189E-15 ) ) ;
#20302=CONICAL_SURFACE ( 'NONE', #4122, 2.055000000000000160, 0.7853981633974717047 ) ;
#20317=ORIENTED_EDGE ( 'NONE', *, *, #1554, .F. ) ;
#20385=DIRECTION ( 'NONE',  ( -0.5000000000000051070, 0.000000000000000000, 0.8660254037844355990 ) ) ;
#20477=( NAMED_UNIT ( * ) SI_UNIT ( $, .STERADIAN. ) SOLID_ANGLE_UNIT ( ) );
#20568=ORIENTED_EDGE ( 'NONE', *, *, #10036, .T. ) ;
#20641=CARTESIAN_POINT ( 'NONE',  ( 2.500000000000002220, -1.178949249685215417, 2.042000000000002036 ) ) ;
#20648=VECTOR ( 'NONE', #8990, 1000.000000000000000 ) ;
#20667=ORIENTED_EDGE ( 'NONE', *, *, #15972, .T. ) ;
#20696=ADVANCED_FACE ( 'NONE', ( #15923 ), #2533, .T. ) ;
#20720=DIRECTION ( 'NONE',  ( -1.000000000000000000, 0.000000000000000000, 0.000000000000000000 ) ) ;
#20766=CARTESIAN_POINT ( 'NONE',  ( 2.500000000000002220, 2.357898499370434386, -3.469446951953614189E-15 ) ) ;
#20817=ADVANCED_FACE ( 'NONE', ( #5055 ), #13585, .F. ) ;
#20880=CYLINDRICAL_SURFACE ( 'NONE', #4037, 2.500000000000000444 ) ;
#20907=DIRECTION ( 'NONE',  ( 1.000000000000000000, 0.000000000000000000, 0.000000000000000000 ) ) ;
#20934=APPLICATION_CONTEXT ( 'automotive_design' ) ;
#20952=ADVANCED_FACE ( 'NONE', ( #3562, #7081 ), #16383, .T. ) ;
#20959=VERTEX_POINT ( 'NONE', #21808 ) ;
#21056=CARTESIAN_POINT ( 'NONE',  ( 0.2500000000000002220, 4.898587196589412829E-16, -3.999999999999979128 ) ) ;
#21154=DIRECTION ( 'NONE',  ( 1.000000000000000000, 0.000000000000000000, 0.000000000000000000 ) ) ;
#21156=AXIS2_PLACEMENT_3D ( 'NONE', #10863, #10728, #6968 ) ;
#21191=EDGE_LOOP ( 'NONE', ( #23192, #15969, #3256, #5690, #17652 ) ) ;
#21211=EDGE_CURVE ( 'NONE', #23797, #2150, #4969, .T. ) ;
#21221=CIRCLE ( 'NONE', #10841, 0.2500000000000002220 ) ;
#21235=VECTOR ( 'NONE', #15823, 1000.000000000000000 ) ;
#21238=VERTEX_POINT ( 'NONE', #12075 ) ;
#21247=CARTESIAN_POINT ( 'NONE',  ( 2.500000000000002220, 2.357898499370434386, -3.469446951953614189E-15 ) ) ;
#21265=DIRECTION ( 'NONE',  ( -1.000000000000000000, 0.000000000000000000, 0.000000000000000000 ) ) ;
#21325=DIRECTION ( 'NONE',  ( 0.000000000000000000, -0.4999999999999991118, 0.8660254037844390407 ) ) ;
#21423=DIRECTION ( 'NONE',  ( -0.7071067811865310304, 0.000000000000000000, 0.7071067811865641151 ) ) ;
#21428=EDGE_LOOP ( 'NONE', ( #18632, #12373, #3961, #18230, #12350 ) ) ;
#21475=DIRECTION ( 'NONE',  ( 0.000000000000000000, 1.000000000000000000, -1.103561164596346103E-15 ) ) ;
#21499=ORIENTED_EDGE ( 'NONE', *, *, #2241, .F. ) ;
#21527=CIRCLE ( 'NONE', #9580, 4.250000000000000000 ) ;
#21545=PRODUCT_DEFINITION_SHAPE ( 'NONE', 'NONE',  #19197 ) ;
#21654=LINE ( 'NONE', #19831, #11478 ) ;
#21687=ORIENTED_EDGE ( 'NONE', *, *, #1850, .F. ) ;
#21734=ORIENTED_EDGE ( 'NONE', *, *, #4041, .T. ) ;
#21801=VECTOR ( 'NONE', #4612, 1000.000000000000000 ) ;
#21808=CARTESIAN_POINT ( 'NONE',  ( 5.000000000000015099, 5.204748896376250699E-16, -4.250000000000000000 ) ) ;
#21809=ADVANCED_FACE ( 'NONE', ( #7492 ), #1942, .F. ) ;
#21817=EDGE_LOOP ( 'NONE', ( #8194, #1549, #6074 ) ) ;
#21847=ORIENTED_EDGE ( 'NONE', *, *, #10221, .F. ) ;
#21854=EDGE_CURVE ( 'NONE', #2150, #23797, #2209, .T. ) ;
#21901=CARTESIAN_POINT ( 'NONE',  ( 2.500000000000015987, -1.768423874527823347, -1.020999999999997687 ) ) ;
#21955=SHAPE_DEFINITION_REPRESENTATION ( #21545, #6508 ) ;
#21971=DIRECTION ( 'NONE',  ( 0.000000000000000000, 0.000000000000000000, 1.000000000000000000 ) ) ;
#21982=DIRECTION ( 'NONE',  ( 0.000000000000000000, -1.000000000000000000, 1.287488025362403787E-15 ) ) ;
#22000=VERTEX_POINT ( 'NONE', #3584 ) ;
#22008=CARTESIAN_POINT ( 'NONE',  ( -31.74999999999994316, 3.061616997868383634E-16, -2.500000000000000444 ) ) ;
#22012=EDGE_CURVE ( 'NONE', #2882, #6583, #15802, .T. ) ;
#22014=ORIENTED_EDGE ( 'NONE', *, *, #14539, .T. ) ;
#22079=DIRECTION ( 'NONE',  ( 0.000000000000000000, 1.000000000000000000, -1.287488025362403787E-15 ) ) ;
#22140=DIRECTION ( 'NONE',  ( 0.000000000000000000, -0.5000000000000009992, -0.8660254037844380415 ) ) ;
#22179=DIRECTION ( 'NONE',  ( -1.000000000000000000, 0.000000000000000000, 0.000000000000000000 ) ) ;
#22213=VERTEX_POINT ( 'NONE', #5748 ) ;
#22216=ADVANCED_FACE ( 'NONE', ( #5502 ), #11222, .F. ) ;
#22223=DIRECTION ( 'NONE',  ( 0.000000000000000000, 0.000000000000000000, -1.000000000000000000 ) ) ;
#22241=PLANE ( 'NONE',  #23456 ) ;
#22270=LINE ( 'NONE', #553, #4984 ) ;
#22346=ORIENTED_EDGE ( 'NONE', *, *, #13032, .F. ) ;
#22369=ORIENTED_EDGE ( 'NONE', *, *, #19903, .T. ) ;
#22373=AXIS2_PLACEMENT_3D ( 'NONE', #1208, #17618, #17404 ) ;
#22387=DIRECTION ( 'NONE',  ( -0.7071067811865310304, 8.659560562355135004E-17, -0.7071067811865641151 ) ) ;
#22389=CARTESIAN_POINT ( 'NONE',  ( 29.55500000000002458, 3.061616997868375746E-16, -2.500000000000000888 ) ) ;
#22406=EDGE_CURVE ( 'NONE', #4361, #12504, #1260, .T. ) ;
#22474=VERTEX_POINT ( 'NONE', #12178 ) ;
#22551=DIRECTION ( 'NONE',  ( -1.000000000000000000, 0.000000000000000000, 0.000000000000000000 ) ) ;
#22587=ORIENTED_EDGE ( 'NONE', *, *, #16781, .T. ) ;
#22607=ADVANCED_FACE ( 'NONE', ( #19924 ), #22241, .F. ) ;
#22654=AXIS2_PLACEMENT_3D ( 'NONE', #17689, #3184, #1153 ) ;
#22696=DIRECTION ( 'NONE',  ( 0.000000000000000000, -0.8660254037844390407, -0.4999999999999992784 ) ) ;
#22717=AXIS2_PLACEMENT_3D ( 'NONE', #4117, #9460, #7878 ) ;
#22780=LINE ( 'NONE', #16862, #20007 ) ;
#22863=EDGE_LOOP ( 'NONE', ( #11743, #23241, #20667, #15452 ) ) ;
#22868=EDGE_CURVE ( 'NONE', #10543, #10801, #12601, .T. ) ;
#22913=DIRECTION ( 'NONE',  ( -1.000000000000000000, 0.000000000000000000, 0.000000000000000000 ) ) ;
#22942=LINE ( 'NONE', #8478, #15658 ) ;
#22961=ORIENTED_EDGE ( 'NONE', *, *, #8714, .F. ) ;
#22997=FACE_OUTER_BOUND ( 'NONE', #3991, .T. ) ;
#23040=CARTESIAN_POINT ( 'NONE',  ( 30.00000000000000000, 0.000000000000000000, 2.054999999999993054 ) ) ;
#23095=CARTESIAN_POINT ( 'NONE',  ( 2.500000000000002220, -1.178949249685218970, -2.041999999999998483 ) ) ;
#23118=DIRECTION ( 'NONE',  ( -1.000000000000000000, 0.000000000000000000, 0.000000000000000000 ) ) ;
#23134=PLANE ( 'NONE',  #23703 ) ;
#23192=ORIENTED_EDGE ( 'NONE', *, *, #18551, .F. ) ;
#23194=DIRECTION ( 'NONE',  ( 0.000000000000000000, -0.4999999999999992228, 0.8660254037844390407 ) ) ;
#23195=EDGE_LOOP ( 'NONE', ( #3690, #3121, #23647, #4363, #8755 ) ) ;
#23241=ORIENTED_EDGE ( 'NONE', *, *, #23704, .T. ) ;
#23247=CARTESIAN_POINT ( 'NONE',  ( 2.500000000000002220, 2.357898499370434386, -3.469446951953614189E-15 ) ) ;
#23256=DIRECTION ( 'NONE',  ( 0.000000000000000000, 0.4999999999999991118, -0.8660254037844391517 ) ) ;
#23266=CARTESIAN_POINT ( 'NONE',  ( 2.500000000000002220, -2.357898499370430834, 3.469446951953614189E-15 ) ) ;
#23295=ORIENTED_EDGE ( 'NONE', *, *, #12194, .T. ) ;
#23303=CARTESIAN_POINT ( 'NONE',  ( 30.00000000000000000, 2.789133085058097101E-16, -2.055000000000006821 ) ) ;
#23349=VERTEX_POINT ( 'NONE', #16993 ) ;
#23456=AXIS2_PLACEMENT_3D ( 'NONE', #16712, #163, #14910 ) ;
#23461=DIRECTION ( 'NONE',  ( 1.000000000000000000, 0.000000000000000000, 0.000000000000000000 ) ) ;
#23472=CARTESIAN_POINT ( 'NONE',  ( 0.2500000000000002220, 0.000000000000000000, 2.081668171172168513E-14 ) ) ;
#23507=ORIENTED_EDGE ( 'NONE', *, *, #2066, .F. ) ;
#23544=EDGE_LOOP ( 'NONE', ( #11997, #7178, #7201, #22587, #22014 ) ) ;
#23550=CARTESIAN_POINT ( 'NONE',  ( 2.500000000000002220, -2.357898499370430834, 3.469446951953614189E-15 ) ) ;
#23553=LINE ( 'NONE', #13942, #2945 ) ;
#23583=CARTESIAN_POINT ( 'NONE',  ( 0.2500000000000002220, 0.000000000000000000, 2.081668171172168513E-14 ) ) ;
#23621=CARTESIAN_POINT ( 'NONE',  ( 0.000000000000000000, -2.357898499370430834, 3.469446951953614189E-15 ) ) ;
#23639=ORIENTED_EDGE ( 'NONE', *, *, #10221, .T. ) ;
#23647=ORIENTED_EDGE ( 'NONE', *, *, #1439, .F. ) ;
#23658=SURFACE_STYLE_USAGE ( .BOTH. , #18647 ) ;
#23703=AXIS2_PLACEMENT_3D ( 'NONE', #8295, #683, #15446 ) ;
#23704=EDGE_CURVE ( 'NONE', #20959, #13509, #15772, .T. ) ;
#23763=CARTESIAN_POINT ( 'NONE',  ( 0.000000000000000000, -1.178949249685215417, 2.042000000000002036 ) ) ;
#23776=CARTESIAN_POINT ( 'NONE',  ( 30.00000000000000000, 0.000000000000000000, -6.938893903907228378E-15 ) ) ;
#23797=VERTEX_POINT ( 'NONE', #12430 ) ;
#23921=COLOUR_RGB('Black',0.12,0.14,0.17);
#23922=FILL_AREA_STYLE_COLOUR('',#23921);
#23923=FILL_AREA_STYLE('',(#23922));
#23924=SURFACE_STYLE_FILL_AREA(#23923);
#23925=SURFACE_SIDE_STYLE('',(#23924));
#23926=SURFACE_STYLE_USAGE(.BOTH.,#23925);
#23927=PRESENTATION_STYLE_ASSIGNMENT((#23926));
ENDSEC;
END-ISO-10303-21;
